ISO-10303-21;
HEADER;
/* Generated by software containing ST-Developer
 * from STEP Tools, Inc. (www.steptools.com) 
 */

FILE_DESCRIPTION(
/* description */ ('Vibration shaker table dummy'),
/* implementation_level */ '2;1');

FILE_NAME(
/* name */ 'Cap Screw - M4x16.step',
/* time_stamp */ '2026-10-27T10:55:14-07:00',
/* author */ (''),
/* organization */ (''),
/* preprocessor_version */ 'ST-DEVELOPER v20.2',
/* originating_system */ 'Autodesk Translation Framework v15.17.0.0',
/* authorisation */ '');

FILE_SCHEMA (('AUTOMOTIVE_DESIGN { 1 0 10303 214 3 1 1 }'));
ENDSEC;

DATA;
#10=MECHANICAL_DESIGN_GEOMETRIC_PRESENTATION_REPRESENTATION('',(#731),#22394);
#569=ORIENTED_CLOSED_SHELL('',*,#9252,.F.);
#572=BREP_WITH_VOIDS('Body1',#9251,(#569));
#582=CONICAL_SURFACE('',#10790,0.325,0.785398163397448);
#583=CONICAL_SURFACE('',#10794,0.335,0.785398163397448);
#584=CONICAL_SURFACE('',#10798,0.21,0.463647609000806);
#585=CONICAL_SURFACE('',#10802,0.18,0.785398163397448);
#639=SHAPE_REPRESENTATION_RELATIONSHIP('SRR','None',#22687,#685);
#685=ADVANCED_BREP_SHAPE_REPRESENTATION('',(#572),#22393);
#731=STYLED_ITEM('',(#22968),#572);
#1059=FACE_BOUND('',#2609,.T.);
#1330=PLANE('',#10788);
#1331=PLANE('',#10796);
#1332=PLANE('',#10804);
#1333=PLANE('',#10805);
#1334=PLANE('',#10806);
#1335=PLANE('',#10807);
#1336=PLANE('',#10808);
#1337=PLANE('',#10809);
#1338=PLANE('',#10810);
#1339=PLANE('',#10811);
#1340=PLANE('',#10812);
#1822=FACE_OUTER_BOUND('',#2604,.T.);
#1823=FACE_OUTER_BOUND('',#2605,.T.);
#1824=FACE_OUTER_BOUND('',#2606,.T.);
#1825=FACE_OUTER_BOUND('',#2607,.T.);
#1826=FACE_OUTER_BOUND('',#2608,.T.);
#1827=FACE_OUTER_BOUND('',#2610,.T.);
#1828=FACE_OUTER_BOUND('',#2611,.T.);
#1829=FACE_OUTER_BOUND('',#2612,.T.);
#1830=FACE_OUTER_BOUND('',#2613,.T.);
#1831=FACE_OUTER_BOUND('',#2614,.T.);
#1832=FACE_OUTER_BOUND('',#2615,.T.);
#1833=FACE_OUTER_BOUND('',#2616,.T.);
#1834=FACE_OUTER_BOUND('',#2617,.T.);
#1835=FACE_OUTER_BOUND('',#2618,.T.);
#1836=FACE_OUTER_BOUND('',#2619,.T.);
#1837=FACE_OUTER_BOUND('',#2620,.T.);
#1838=FACE_OUTER_BOUND('',#2621,.T.);
#2604=EDGE_LOOP('',(#8442));
#2605=EDGE_LOOP('',(#8443,#8444,#8445,#8446));
#2606=EDGE_LOOP('',(#8447,#8448,#8449,#8450));
#2607=EDGE_LOOP('',(#8451,#8452,#8453,#8454));
#2608=EDGE_LOOP('',(#8455));
#2609=EDGE_LOOP('',(#8456));
#2610=EDGE_LOOP('',(#8457,#8458,#8459,#8460));
#2611=EDGE_LOOP('',(#8461,#8462,#8463,#8464));
#2612=EDGE_LOOP('',(#8465,#8466,#8467,#8468));
#2613=EDGE_LOOP('',(#8469));
#2614=EDGE_LOOP('',(#8470,#8471,#8472,#8473));
#2615=EDGE_LOOP('',(#8474,#8475,#8476,#8477));
#2616=EDGE_LOOP('',(#8478,#8479,#8480,#8481));
#2617=EDGE_LOOP('',(#8482,#8483,#8484,#8485));
#2618=EDGE_LOOP('',(#8486,#8487,#8488,#8489));
#2619=EDGE_LOOP('',(#8490,#8491,#8492,#8493));
#2620=EDGE_LOOP('',(#8494,#8495,#8496,#8497,#8498,#8499));
#2621=EDGE_LOOP('',(#8500,#8501,#8502,#8503,#8504,#8505));
#3217=LINE('',#22093,#3836);
#3218=LINE('',#22097,#3837);
#3219=LINE('',#22101,#3838);
#3220=LINE('',#22108,#3839);
#3221=LINE('',#22112,#3840);
#3222=LINE('',#22116,#3841);
#3223=LINE('',#22121,#3842);
#3224=LINE('',#22123,#3843);
#3225=LINE('',#22125,#3844);
#3226=LINE('',#22126,#3845);
#3227=LINE('',#22129,#3846);
#3228=LINE('',#22131,#3847);
#3229=LINE('',#22132,#3848);
#3230=LINE('',#22135,#3849);
#3231=LINE('',#22137,#3850);
#3232=LINE('',#22138,#3851);
#3233=LINE('',#22141,#3852);
#3234=LINE('',#22143,#3853);
#3235=LINE('',#22144,#3854);
#3236=LINE('',#22147,#3855);
#3237=LINE('',#22149,#3856);
#3238=LINE('',#22150,#3857);
#3239=LINE('',#22152,#3858);
#3240=LINE('',#22153,#3859);
#3836=VECTOR('',#13609,0.325);
#3837=VECTOR('',#13614,0.35);
#3838=VECTOR('',#13619,0.335);
#3839=VECTOR('',#13628,0.21);
#3840=VECTOR('',#13633,0.2);
#3841=VECTOR('',#13638,0.18);
#3842=VECTOR('',#13643,1.);
#3843=VECTOR('',#13644,1.);
#3844=VECTOR('',#13645,1.);
#3845=VECTOR('',#13646,1.);
#3846=VECTOR('',#13649,1.);
#3847=VECTOR('',#13650,1.);
#3848=VECTOR('',#13651,1.);
#3849=VECTOR('',#13654,1.);
#3850=VECTOR('',#13655,1.);
#3851=VECTOR('',#13656,1.);
#3852=VECTOR('',#13659,1.);
#3853=VECTOR('',#13660,1.);
#3854=VECTOR('',#13661,1.);
#3855=VECTOR('',#13664,1.);
#3856=VECTOR('',#13665,1.);
#3857=VECTOR('',#13666,1.);
#3858=VECTOR('',#13669,1.);
#3859=VECTOR('',#13670,1.);
#4359=CIRCLE('',#10789,0.3);
#4360=CIRCLE('',#10791,0.35);
#4361=CIRCLE('',#10793,0.35);
#4362=CIRCLE('',#10795,0.32);
#4363=CIRCLE('',#10797,0.22);
#4364=CIRCLE('',#10799,0.1954);
#4365=CIRCLE('',#10801,0.1954);
#4366=CIRCLE('',#10803,0.16);
#5096=VERTEX_POINT('',#22088);
#5097=VERTEX_POINT('',#22091);
#5098=VERTEX_POINT('',#22095);
#5099=VERTEX_POINT('',#22099);
#5100=VERTEX_POINT('',#22103);
#5101=VERTEX_POINT('',#22106);
#5102=VERTEX_POINT('',#22110);
#5103=VERTEX_POINT('',#22114);
#5104=VERTEX_POINT('',#22119);
#5105=VERTEX_POINT('',#22120);
#5106=VERTEX_POINT('',#22122);
#5107=VERTEX_POINT('',#22124);
#5108=VERTEX_POINT('',#22128);
#5109=VERTEX_POINT('',#22130);
#5110=VERTEX_POINT('',#22134);
#5111=VERTEX_POINT('',#22136);
#5112=VERTEX_POINT('',#22140);
#5113=VERTEX_POINT('',#22142);
#5114=VERTEX_POINT('',#22146);
#5115=VERTEX_POINT('',#22148);
#6214=EDGE_CURVE('',#5096,#5096,#4359,.T.);
#6215=EDGE_CURVE('',#5097,#5097,#4360,.T.);
#6216=EDGE_CURVE('',#5097,#5096,#3217,.T.);
#6217=EDGE_CURVE('',#5098,#5098,#4361,.T.);
#6218=EDGE_CURVE('',#5098,#5097,#3218,.T.);
#6219=EDGE_CURVE('',#5099,#5099,#4362,.T.);
#6220=EDGE_CURVE('',#5099,#5098,#3219,.T.);
#6221=EDGE_CURVE('',#5100,#5100,#4363,.T.);
#6222=EDGE_CURVE('',#5101,#5101,#4364,.F.);
#6223=EDGE_CURVE('',#5101,#5100,#3220,.T.);
#6224=EDGE_CURVE('',#5102,#5102,#4365,.F.);
#6225=EDGE_CURVE('',#5102,#5101,#3221,.T.);
#6226=EDGE_CURVE('',#5103,#5103,#4366,.T.);
#6227=EDGE_CURVE('',#5103,#5102,#3222,.T.);
#6228=EDGE_CURVE('',#5104,#5105,#3223,.T.);
#6229=EDGE_CURVE('',#5105,#5106,#3224,.T.);
#6230=EDGE_CURVE('',#5106,#5107,#3225,.T.);
#6231=EDGE_CURVE('',#5104,#5107,#3226,.T.);
#6232=EDGE_CURVE('',#5105,#5108,#3227,.T.);
#6233=EDGE_CURVE('',#5108,#5109,#3228,.T.);
#6234=EDGE_CURVE('',#5109,#5106,#3229,.T.);
#6235=EDGE_CURVE('',#5108,#5110,#3230,.T.);
#6236=EDGE_CURVE('',#5110,#5111,#3231,.T.);
#6237=EDGE_CURVE('',#5111,#5109,#3232,.T.);
#6238=EDGE_CURVE('',#5110,#5112,#3233,.T.);
#6239=EDGE_CURVE('',#5112,#5113,#3234,.T.);
#6240=EDGE_CURVE('',#5113,#5111,#3235,.T.);
#6241=EDGE_CURVE('',#5112,#5114,#3236,.T.);
#6242=EDGE_CURVE('',#5114,#5115,#3237,.T.);
#6243=EDGE_CURVE('',#5115,#5113,#3238,.T.);
#6244=EDGE_CURVE('',#5114,#5104,#3239,.T.);
#6245=EDGE_CURVE('',#5107,#5115,#3240,.T.);
#8442=ORIENTED_EDGE('',*,*,#6214,.F.);
#8443=ORIENTED_EDGE('',*,*,#6215,.F.);
#8444=ORIENTED_EDGE('',*,*,#6216,.T.);
#8445=ORIENTED_EDGE('',*,*,#6214,.T.);
#8446=ORIENTED_EDGE('',*,*,#6216,.F.);
#8447=ORIENTED_EDGE('',*,*,#6217,.F.);
#8448=ORIENTED_EDGE('',*,*,#6218,.T.);
#8449=ORIENTED_EDGE('',*,*,#6215,.T.);
#8450=ORIENTED_EDGE('',*,*,#6218,.F.);
#8451=ORIENTED_EDGE('',*,*,#6219,.F.);
#8452=ORIENTED_EDGE('',*,*,#6220,.T.);
#8453=ORIENTED_EDGE('',*,*,#6217,.T.);
#8454=ORIENTED_EDGE('',*,*,#6220,.F.);
#8455=ORIENTED_EDGE('',*,*,#6219,.T.);
#8456=ORIENTED_EDGE('',*,*,#6221,.F.);
#8457=ORIENTED_EDGE('',*,*,#6222,.F.);
#8458=ORIENTED_EDGE('',*,*,#6223,.T.);
#8459=ORIENTED_EDGE('',*,*,#6221,.T.);
#8460=ORIENTED_EDGE('',*,*,#6223,.F.);
#8461=ORIENTED_EDGE('',*,*,#6224,.F.);
#8462=ORIENTED_EDGE('',*,*,#6225,.T.);
#8463=ORIENTED_EDGE('',*,*,#6222,.T.);
#8464=ORIENTED_EDGE('',*,*,#6225,.F.);
#8465=ORIENTED_EDGE('',*,*,#6226,.F.);
#8466=ORIENTED_EDGE('',*,*,#6227,.T.);
#8467=ORIENTED_EDGE('',*,*,#6224,.T.);
#8468=ORIENTED_EDGE('',*,*,#6227,.F.);
#8469=ORIENTED_EDGE('',*,*,#6226,.T.);
#8470=ORIENTED_EDGE('',*,*,#6228,.T.);
#8471=ORIENTED_EDGE('',*,*,#6229,.T.);
#8472=ORIENTED_EDGE('',*,*,#6230,.T.);
#8473=ORIENTED_EDGE('',*,*,#6231,.F.);
#8474=ORIENTED_EDGE('',*,*,#6232,.T.);
#8475=ORIENTED_EDGE('',*,*,#6233,.T.);
#8476=ORIENTED_EDGE('',*,*,#6234,.T.);
#8477=ORIENTED_EDGE('',*,*,#6229,.F.);
#8478=ORIENTED_EDGE('',*,*,#6235,.T.);
#8479=ORIENTED_EDGE('',*,*,#6236,.T.);
#8480=ORIENTED_EDGE('',*,*,#6237,.T.);
#8481=ORIENTED_EDGE('',*,*,#6233,.F.);
#8482=ORIENTED_EDGE('',*,*,#6238,.T.);
#8483=ORIENTED_EDGE('',*,*,#6239,.T.);
#8484=ORIENTED_EDGE('',*,*,#6240,.T.);
#8485=ORIENTED_EDGE('',*,*,#6236,.F.);
#8486=ORIENTED_EDGE('',*,*,#6241,.T.);
#8487=ORIENTED_EDGE('',*,*,#6242,.T.);
#8488=ORIENTED_EDGE('',*,*,#6243,.T.);
#8489=ORIENTED_EDGE('',*,*,#6239,.F.);
#8490=ORIENTED_EDGE('',*,*,#6244,.T.);
#8491=ORIENTED_EDGE('',*,*,#6231,.T.);
#8492=ORIENTED_EDGE('',*,*,#6245,.T.);
#8493=ORIENTED_EDGE('',*,*,#6242,.F.);
#8494=ORIENTED_EDGE('',*,*,#6244,.F.);
#8495=ORIENTED_EDGE('',*,*,#6241,.F.);
#8496=ORIENTED_EDGE('',*,*,#6238,.F.);
#8497=ORIENTED_EDGE('',*,*,#6235,.F.);
#8498=ORIENTED_EDGE('',*,*,#6232,.F.);
#8499=ORIENTED_EDGE('',*,*,#6228,.F.);
#8500=ORIENTED_EDGE('',*,*,#6245,.F.);
#8501=ORIENTED_EDGE('',*,*,#6230,.F.);
#8502=ORIENTED_EDGE('',*,*,#6234,.F.);
#8503=ORIENTED_EDGE('',*,*,#6237,.F.);
#8504=ORIENTED_EDGE('',*,*,#6240,.F.);
#8505=ORIENTED_EDGE('',*,*,#6243,.F.);
#8704=CYLINDRICAL_SURFACE('',#10792,0.35);
#8705=CYLINDRICAL_SURFACE('',#10800,0.1954);
#9187=ADVANCED_FACE('',(#1822),#1330,.T.);
#9188=ADVANCED_FACE('',(#1823),#582,.T.);
#9189=ADVANCED_FACE('',(#1824),#8704,.T.);
#9190=ADVANCED_FACE('',(#1825),#583,.T.);
#9191=ADVANCED_FACE('',(#1826,#1059),#1331,.T.);
#9192=ADVANCED_FACE('',(#1827),#584,.T.);
#9193=ADVANCED_FACE('',(#1828),#8705,.T.);
#9194=ADVANCED_FACE('',(#1829),#585,.T.);
#9195=ADVANCED_FACE('',(#1830),#1332,.T.);
#9196=ADVANCED_FACE('',(#1831),#1333,.F.);
#9197=ADVANCED_FACE('',(#1832),#1334,.F.);
#9198=ADVANCED_FACE('',(#1833),#1335,.F.);
#9199=ADVANCED_FACE('',(#1834),#1336,.F.);
#9200=ADVANCED_FACE('',(#1835),#1337,.F.);
#9201=ADVANCED_FACE('',(#1836),#1338,.F.);
#9202=ADVANCED_FACE('',(#1837),#1339,.F.);
#9203=ADVANCED_FACE('',(#1838),#1340,.F.);
#9251=CLOSED_SHELL('',(#9187,#9188,#9189,#9190,#9191,#9192,#9193,#9194,
#9195));
#9252=CLOSED_SHELL('',(#9196,#9197,#9198,#9199,#9200,#9201,#9202,#9203));
#10787=AXIS2_PLACEMENT_3D('',#22086,#13599,#13600);
#10788=AXIS2_PLACEMENT_3D('',#22087,#13601,#13602);
#10789=AXIS2_PLACEMENT_3D('',#22089,#13603,#13604);
#10790=AXIS2_PLACEMENT_3D('',#22090,#13605,#13606);
#10791=AXIS2_PLACEMENT_3D('',#22092,#13607,#13608);
#10792=AXIS2_PLACEMENT_3D('',#22094,#13610,#13611);
#10793=AXIS2_PLACEMENT_3D('',#22096,#13612,#13613);
#10794=AXIS2_PLACEMENT_3D('',#22098,#13615,#13616);
#10795=AXIS2_PLACEMENT_3D('',#22100,#13617,#13618);
#10796=AXIS2_PLACEMENT_3D('',#22102,#13620,#13621);
#10797=AXIS2_PLACEMENT_3D('',#22104,#13622,#13623);
#10798=AXIS2_PLACEMENT_3D('',#22105,#13624,#13625);
#10799=AXIS2_PLACEMENT_3D('',#22107,#13626,#13627);
#10800=AXIS2_PLACEMENT_3D('',#22109,#13629,#13630);
#10801=AXIS2_PLACEMENT_3D('',#22111,#13631,#13632);
#10802=AXIS2_PLACEMENT_3D('',#22113,#13634,#13635);
#10803=AXIS2_PLACEMENT_3D('',#22115,#13636,#13637);
#10804=AXIS2_PLACEMENT_3D('',#22117,#13639,#13640);
#10805=AXIS2_PLACEMENT_3D('',#22118,#13641,#13642);
#10806=AXIS2_PLACEMENT_3D('',#22127,#13647,#13648);
#10807=AXIS2_PLACEMENT_3D('',#22133,#13652,#13653);
#10808=AXIS2_PLACEMENT_3D('',#22139,#13657,#13658);
#10809=AXIS2_PLACEMENT_3D('',#22145,#13662,#13663);
#10810=AXIS2_PLACEMENT_3D('',#22151,#13667,#13668);
#10811=AXIS2_PLACEMENT_3D('',#22154,#13671,#13672);
#10812=AXIS2_PLACEMENT_3D('',#22155,#13673,#13674);
#13599=DIRECTION('axis',(0.,0.,1.));
#13600=DIRECTION('refdir',(1.,0.,0.));
#13601=DIRECTION('center_axis',(0.,1.,0.));
#13602=DIRECTION('ref_axis',(0.,0.,1.));
#13603=DIRECTION('center_axis',(0.,-1.,0.));
#13604=DIRECTION('ref_axis',(1.,0.,0.));
#13605=DIRECTION('center_axis',(0.,-1.,0.));
#13606=DIRECTION('ref_axis',(1.,0.,0.));
#13607=DIRECTION('center_axis',(0.,-1.,0.));
#13608=DIRECTION('ref_axis',(1.,0.,0.));
#13609=DIRECTION('',(0.707106781186547,0.707106781186548,8.65956056235493E-17));
#13610=DIRECTION('center_axis',(0.,-1.,0.));
#13611=DIRECTION('ref_axis',(1.,0.,0.));
#13612=DIRECTION('center_axis',(0.,-1.,0.));
#13613=DIRECTION('ref_axis',(1.,0.,0.));
#13614=DIRECTION('',(0.,1.,0.));
#13615=DIRECTION('center_axis',(0.,1.,0.));
#13616=DIRECTION('ref_axis',(1.,0.,0.));
#13617=DIRECTION('center_axis',(0.,-1.,0.));
#13618=DIRECTION('ref_axis',(1.,0.,0.));
#13619=DIRECTION('',(-0.707106781186547,0.707106781186548,-8.65956056235493E-17));
#13620=DIRECTION('center_axis',(0.,-1.,0.));
#13621=DIRECTION('ref_axis',(0.,0.,-1.));
#13622=DIRECTION('center_axis',(0.,-1.,0.));
#13623=DIRECTION('ref_axis',(1.,0.,0.));
#13624=DIRECTION('center_axis',(0.,1.,0.));
#13625=DIRECTION('ref_axis',(1.,0.,0.));
#13626=DIRECTION('center_axis',(0.,1.,0.));
#13627=DIRECTION('ref_axis',(1.,0.,0.));
#13628=DIRECTION('',(-0.447213595499958,0.894427190999916,-5.47678698264203E-17));
#13629=DIRECTION('center_axis',(0.,-1.,0.));
#13630=DIRECTION('ref_axis',(1.,0.,0.));
#13631=DIRECTION('center_axis',(0.,1.,0.));
#13632=DIRECTION('ref_axis',(1.,0.,0.));
#13633=DIRECTION('',(0.,1.,0.));
#13634=DIRECTION('center_axis',(0.,1.,0.));
#13635=DIRECTION('ref_axis',(1.,0.,0.));
#13636=DIRECTION('center_axis',(0.,-1.,0.));
#13637=DIRECTION('ref_axis',(1.,0.,0.));
#13638=DIRECTION('',(-0.707106781186547,0.707106781186548,-8.65956056235493E-17));
#13639=DIRECTION('center_axis',(0.,-1.,0.));
#13640=DIRECTION('ref_axis',(0.,0.,-1.));
#13641=DIRECTION('center_axis',(0.866025403784439,0.,-0.5));
#13642=DIRECTION('ref_axis',(0.5,0.,0.866025403784439));
#13643=DIRECTION('',(-0.5,0.,-0.866025403784439));
#13644=DIRECTION('',(0.,-1.,0.));
#13645=DIRECTION('',(0.5,0.,0.866025403784439));
#13646=DIRECTION('',(0.,-1.,0.));
#13647=DIRECTION('center_axis',(1.60246890531964E-16,0.,-1.));
#13648=DIRECTION('ref_axis',(1.,0.,1.60246890531964E-16));
#13649=DIRECTION('',(-1.,0.,-1.60246890531964E-16));
#13650=DIRECTION('',(0.,-1.,0.));
#13651=DIRECTION('',(1.,0.,1.60246890531964E-16));
#13652=DIRECTION('center_axis',(-0.866025403784439,0.,-0.5));
#13653=DIRECTION('ref_axis',(0.5,0.,-0.866025403784439));
#13654=DIRECTION('',(-0.5,0.,0.866025403784439));
#13655=DIRECTION('',(0.,-1.,0.));
#13656=DIRECTION('',(0.5,0.,-0.866025403784439));
#13657=DIRECTION('center_axis',(-0.866025403784439,0.,0.5));
#13658=DIRECTION('ref_axis',(-0.5,0.,-0.866025403784439));
#13659=DIRECTION('',(0.5,0.,0.866025403784439));
#13660=DIRECTION('',(0.,-1.,0.));
#13661=DIRECTION('',(-0.5,0.,-0.866025403784439));
#13662=DIRECTION('center_axis',(-1.60246890531964E-16,0.,1.));
#13663=DIRECTION('ref_axis',(-1.,0.,-1.60246890531964E-16));
#13664=DIRECTION('',(1.,0.,1.60246890531964E-16));
#13665=DIRECTION('',(0.,-1.,0.));
#13666=DIRECTION('',(-1.,0.,-1.60246890531964E-16));
#13667=DIRECTION('center_axis',(0.866025403784439,0.,0.5));
#13668=DIRECTION('ref_axis',(-0.5,0.,0.866025403784439));
#13669=DIRECTION('',(0.5,0.,-0.866025403784439));
#13670=DIRECTION('',(-0.5,0.,0.866025403784439));
#13671=DIRECTION('center_axis',(0.,1.,0.));
#13672=DIRECTION('ref_axis',(1.,0.,0.));
#13673=DIRECTION('center_axis',(0.,-1.,0.));
#13674=DIRECTION('ref_axis',(0.,0.,-1.));
#22086=CARTESIAN_POINT('',(0.,0.,0.));
#22087=CARTESIAN_POINT('Origin',(0.3,0.4,0.));
#22088=CARTESIAN_POINT('',(-0.3,0.4,-3.67394039744206E-17));
#22089=CARTESIAN_POINT('Origin',(0.,0.4,0.));
#22090=CARTESIAN_POINT('Origin',(0.,0.375,0.));
#22091=CARTESIAN_POINT('',(-0.35,0.35,-4.28626379701573E-17));
#22092=CARTESIAN_POINT('Origin',(0.,0.35,0.));
#22093=CARTESIAN_POINT('',(-0.325,0.375,-3.9801020972289E-17));
#22094=CARTESIAN_POINT('Origin',(0.,0.19,0.));
#22095=CARTESIAN_POINT('',(-0.35,0.03,-4.28626379701574E-17));
#22096=CARTESIAN_POINT('Origin',(0.,0.03,0.));
#22097=CARTESIAN_POINT('',(-0.35,0.19,-4.28626379701574E-17));
#22098=CARTESIAN_POINT('Origin',(0.,0.0149999999999999,0.));
#22099=CARTESIAN_POINT('',(-0.32,-3.29597460435593E-17,-3.91886975727153E-17));
#22100=CARTESIAN_POINT('Origin',(0.,0.,0.));
#22101=CARTESIAN_POINT('',(-0.335,0.0149999999999999,-4.10256677714363E-17));
#22102=CARTESIAN_POINT('Origin',(0.22,0.,0.));
#22103=CARTESIAN_POINT('',(-0.22,-6.93889390390723E-18,-2.69422295812418E-17));
#22104=CARTESIAN_POINT('Origin',(0.,0.,0.));
#22105=CARTESIAN_POINT('Origin',(0.,-0.02,0.));
#22106=CARTESIAN_POINT('',(-0.1954,-0.0492,2.39295984553393E-17));
#22107=CARTESIAN_POINT('Origin',(0.,-0.0492,0.));
#22108=CARTESIAN_POINT('',(-0.21,-0.02,-2.57175827820944E-17));
#22109=CARTESIAN_POINT('Origin',(0.,-0.8,0.));
#22110=CARTESIAN_POINT('',(-0.1954,-1.5646,2.39295984553393E-17));
#22111=CARTESIAN_POINT('Origin',(0.,-1.5646,0.));
#22112=CARTESIAN_POINT('',(-0.1954,-0.8,-2.39295984553393E-17));
#22113=CARTESIAN_POINT('Origin',(0.,-1.58,0.));
#22114=CARTESIAN_POINT('',(-0.16,-1.6,-1.95943487863577E-17));
#22115=CARTESIAN_POINT('Origin',(0.,-1.6,0.));
#22116=CARTESIAN_POINT('',(-0.18,-1.58,-2.20436423846524E-17));
#22117=CARTESIAN_POINT('Origin',(0.,-1.6,0.));
#22118=CARTESIAN_POINT('Origin',(0.0866025403784439,-0.4,-0.15));
#22119=CARTESIAN_POINT('',(0.173205080756888,-0.4,0.));
#22120=CARTESIAN_POINT('',(0.0866025403784439,-0.4,-0.15));
#22121=CARTESIAN_POINT('',(0.173205080756888,-0.4,0.));
#22122=CARTESIAN_POINT('',(0.0866025403784439,-0.64,-0.15));
#22123=CARTESIAN_POINT('',(0.0866025403784439,-0.4,-0.15));
#22124=CARTESIAN_POINT('',(0.173205080756888,-0.64,0.));
#22125=CARTESIAN_POINT('',(0.173205080756888,-0.64,0.));
#22126=CARTESIAN_POINT('',(0.173205080756888,-0.4,0.));
#22127=CARTESIAN_POINT('Origin',(-0.0866025403784438,-0.4,-0.15));
#22128=CARTESIAN_POINT('',(-0.0866025403784438,-0.4,-0.15));
#22129=CARTESIAN_POINT('',(0.0866025403784439,-0.4,-0.15));
#22130=CARTESIAN_POINT('',(-0.0866025403784438,-0.64,-0.15));
#22131=CARTESIAN_POINT('',(-0.0866025403784438,-0.4,-0.15));
#22132=CARTESIAN_POINT('',(0.0866025403784439,-0.64,-0.15));
#22133=CARTESIAN_POINT('Origin',(-0.173205080756888,-0.4,-2.77555756156289E-17));
#22134=CARTESIAN_POINT('',(-0.173205080756888,-0.4,-2.12115047744981E-17));
#22135=CARTESIAN_POINT('',(-0.0866025403784438,-0.4,-0.15));
#22136=CARTESIAN_POINT('',(-0.173205080756888,-0.64,-2.77555756156289E-17));
#22137=CARTESIAN_POINT('',(-0.173205080756888,-0.4,-2.12115047744981E-17));
#22138=CARTESIAN_POINT('',(-0.0866025403784438,-0.64,-0.15));
#22139=CARTESIAN_POINT('Origin',(-0.0866025403784439,-0.4,0.15));
#22140=CARTESIAN_POINT('',(-0.0866025403784439,-0.4,0.15));
#22141=CARTESIAN_POINT('',(-0.173205080756888,-0.4,-2.12115047744981E-17));
#22142=CARTESIAN_POINT('',(-0.0866025403784439,-0.64,0.15));
#22143=CARTESIAN_POINT('',(-0.0866025403784439,-0.4,0.15));
#22144=CARTESIAN_POINT('',(-0.173205080756888,-0.64,-2.12115047744981E-17));
#22145=CARTESIAN_POINT('Origin',(0.0866025403784439,-0.4,0.15));
#22146=CARTESIAN_POINT('',(0.0866025403784439,-0.4,0.15));
#22147=CARTESIAN_POINT('',(-0.0866025403784439,-0.4,0.15));
#22148=CARTESIAN_POINT('',(0.0866025403784439,-0.64,0.15));
#22149=CARTESIAN_POINT('',(0.0866025403784439,-0.4,0.15));
#22150=CARTESIAN_POINT('',(-0.0866025403784439,-0.64,0.15));
#22151=CARTESIAN_POINT('Origin',(0.173205080756888,-0.4,0.));
#22152=CARTESIAN_POINT('',(0.0866025403784439,-0.4,0.15));
#22153=CARTESIAN_POINT('',(0.0866025403784439,-0.64,0.15));
#22154=CARTESIAN_POINT('Origin',(0.,-0.4,-2.77555756156289E-17));
#22155=CARTESIAN_POINT('Origin',(0.,-0.64,-2.77555756156289E-17));
#22342=UNCERTAINTY_MEASURE_WITH_UNIT(LENGTH_MEASURE(0.001),#22395,
'DISTANCE_ACCURACY_VALUE',
'Maximum model space distance between geometric entities at asserted c
onnectivities');
#22343=UNCERTAINTY_MEASURE_WITH_UNIT(LENGTH_MEASURE(0.001),#22395,
'DISTANCE_ACCURACY_VALUE',
'Maximum model space distance between geometric entities at asserted c
onnectivities');
#22393=(
GEOMETRIC_REPRESENTATION_CONTEXT(3)
GLOBAL_UNCERTAINTY_ASSIGNED_CONTEXT((#22342))
GLOBAL_UNIT_ASSIGNED_CONTEXT((#22395,#22397,#22398))
REPRESENTATION_CONTEXT('','3D')
);
#22394=(
GEOMETRIC_REPRESENTATION_CONTEXT(3)
GLOBAL_UNCERTAINTY_ASSIGNED_CONTEXT((#22343))
GLOBAL_UNIT_ASSIGNED_CONTEXT((#22395,#22397,#22398))
REPRESENTATION_CONTEXT('','3D')
);
#22395=(
LENGTH_UNIT()
NAMED_UNIT(*)
SI_UNIT(.CENTI.,.METRE.)
);
#22397=(
NAMED_UNIT(*)
PLANE_ANGLE_UNIT()
SI_UNIT($,.RADIAN.)
);
#22398=(
NAMED_UNIT(*)
SI_UNIT($,.STERADIAN.)
SOLID_ANGLE_UNIT()
);
#22448=SHAPE_DEFINITION_REPRESENTATION(#22500,#22687);
#22500=PRODUCT_DEFINITION_SHAPE('',$,#22738);
#22687=SHAPE_REPRESENTATION('',(#10787),#22393);
#22688=PRODUCT_DEFINITION_CONTEXT('part definition',#22840,'design');
#22738=PRODUCT_DEFINITION('Cap Screw - M4x16','Cap Screw - M4x16',#22788,
#22688);
#22788=PRODUCT_DEFINITION_FORMATION('',$,#22891);
#22840=APPLICATION_CONTEXT(
'Core Data for Automotive Mechanical Design Process');
#22841=PRODUCT_CONTEXT('part definition',#22840,'mechanical');
#22891=PRODUCT('Cap Screw - M4x16','Cap Screw - M4x16',
'Cap Screw - M4x16',(#22841));
#22962=COLOUR_RGB('Black',0.12,0.14,0.17);
#22963=FILL_AREA_STYLE_COLOUR('',#22962);
#22964=FILL_AREA_STYLE('',(#22963));
#22965=SURFACE_STYLE_FILL_AREA(#22964);
#22966=SURFACE_SIDE_STYLE('',(#22965));
#22967=SURFACE_STYLE_USAGE(.BOTH.,#22966);
#22968=PRESENTATION_STYLE_ASSIGNMENT((#22967));
ENDSEC;
END-ISO-10303-21;
